ISO-10303-21;
HEADER;
/* Generated by software containing ST-Developer
 * from STEP Tools, Inc. (www.steptools.com) 
 */

FILE_DESCRIPTION(
/* description */ ('Lever-operated bar clamp (toggle)'),
/* implementation_level */ '2;1');

FILE_NAME(
/* name */ 'Cap Screw - M4x16.step',
/* time_stamp */ '2026-10-28T03:25:02-07:00',
/* author */ (''),
/* organization */ (''),
/* preprocessor_version */ 'ST-DEVELOPER v20.2',
/* originating_system */ 'Autodesk Translation Framework v15.17.0.0',
/* authorisation */ '');

FILE_SCHEMA (('AUTOMOTIVE_DESIGN { 1 0 10303 214 3 1 1 }'));
ENDSEC;

DATA;
#10=MECHANICAL_DESIGN_GEOMETRIC_PRESENTATION_REPRESENTATION('',(#448),#12413);
#320=CONICAL_SURFACE('',#7705,0.325,0.785398163397448);
#321=CONICAL_SURFACE('',#7709,0.335,0.785398163397448);
#322=CONICAL_SURFACE('',#7713,0.21,0.463647609000806);
#323=CONICAL_SURFACE('',#7717,0.18,0.785398163397448);
#329=ORIENTED_CLOSED_SHELL('',*,#6611,.F.);
#333=BREP_WITH_VOIDS('Body1',#6610,(#329));
#364=SHAPE_REPRESENTATION_RELATIONSHIP('SRR','None',#12606,#402);
#402=ADVANCED_BREP_SHAPE_REPRESENTATION('',(#333),#12403);
#448=STYLED_ITEM('',(#12876),#333);
#635=FACE_BOUND('',#1763,.T.);
#836=PLANE('',#7703);
#837=PLANE('',#7711);
#838=PLANE('',#7719);
#839=PLANE('',#7720);
#840=PLANE('',#7721);
#841=PLANE('',#7722);
#842=PLANE('',#7723);
#843=PLANE('',#7724);
#844=PLANE('',#7725);
#845=PLANE('',#7726);
#846=PLANE('',#7727);
#1217=FACE_OUTER_BOUND('',#1758,.T.);
#1218=FACE_OUTER_BOUND('',#1759,.T.);
#1219=FACE_OUTER_BOUND('',#1760,.T.);
#1220=FACE_OUTER_BOUND('',#1761,.T.);
#1221=FACE_OUTER_BOUND('',#1762,.T.);
#1222=FACE_OUTER_BOUND('',#1764,.T.);
#1223=FACE_OUTER_BOUND('',#1765,.T.);
#1224=FACE_OUTER_BOUND('',#1766,.T.);
#1225=FACE_OUTER_BOUND('',#1767,.T.);
#1226=FACE_OUTER_BOUND('',#1768,.T.);
#1227=FACE_OUTER_BOUND('',#1769,.T.);
#1228=FACE_OUTER_BOUND('',#1770,.T.);
#1229=FACE_OUTER_BOUND('',#1771,.T.);
#1230=FACE_OUTER_BOUND('',#1772,.T.);
#1231=FACE_OUTER_BOUND('',#1773,.T.);
#1232=FACE_OUTER_BOUND('',#1774,.T.);
#1233=FACE_OUTER_BOUND('',#1775,.T.);
#1758=EDGE_LOOP('',(#5729));
#1759=EDGE_LOOP('',(#5730,#5731,#5732,#5733));
#1760=EDGE_LOOP('',(#5734,#5735,#5736,#5737));
#1761=EDGE_LOOP('',(#5738,#5739,#5740,#5741));
#1762=EDGE_LOOP('',(#5742));
#1763=EDGE_LOOP('',(#5743));
#1764=EDGE_LOOP('',(#5744,#5745,#5746,#5747));
#1765=EDGE_LOOP('',(#5748,#5749,#5750,#5751));
#1766=EDGE_LOOP('',(#5752,#5753,#5754,#5755));
#1767=EDGE_LOOP('',(#5756));
#1768=EDGE_LOOP('',(#5757,#5758,#5759,#5760));
#1769=EDGE_LOOP('',(#5761,#5762,#5763,#5764));
#1770=EDGE_LOOP('',(#5765,#5766,#5767,#5768));
#1771=EDGE_LOOP('',(#5769,#5770,#5771,#5772));
#1772=EDGE_LOOP('',(#5773,#5774,#5775,#5776));
#1773=EDGE_LOOP('',(#5777,#5778,#5779,#5780));
#1774=EDGE_LOOP('',(#5781,#5782,#5783,#5784,#5785,#5786));
#1775=EDGE_LOOP('',(#5787,#5788,#5789,#5790,#5791,#5792));
#2191=LINE('',#11917,#2632);
#2192=LINE('',#11921,#2633);
#2193=LINE('',#11925,#2634);
#2194=LINE('',#11932,#2635);
#2195=LINE('',#11936,#2636);
#2196=LINE('',#11940,#2637);
#2197=LINE('',#11945,#2638);
#2198=LINE('',#11947,#2639);
#2199=LINE('',#11949,#2640);
#2200=LINE('',#11950,#2641);
#2201=LINE('',#11953,#2642);
#2202=LINE('',#11955,#2643);
#2203=LINE('',#11956,#2644);
#2204=LINE('',#11959,#2645);
#2205=LINE('',#11961,#2646);
#2206=LINE('',#11962,#2647);
#2207=LINE('',#11965,#2648);
#2208=LINE('',#11967,#2649);
#2209=LINE('',#11968,#2650);
#2210=LINE('',#11971,#2651);
#2211=LINE('',#11973,#2652);
#2212=LINE('',#11974,#2653);
#2213=LINE('',#11976,#2654);
#2214=LINE('',#11977,#2655);
#2632=VECTOR('',#9570,0.325);
#2633=VECTOR('',#9575,0.35);
#2634=VECTOR('',#9580,0.335);
#2635=VECTOR('',#9589,0.21);
#2636=VECTOR('',#9594,0.2);
#2637=VECTOR('',#9599,0.18);
#2638=VECTOR('',#9604,1.);
#2639=VECTOR('',#9605,1.);
#2640=VECTOR('',#9606,1.);
#2641=VECTOR('',#9607,1.);
#2642=VECTOR('',#9610,1.);
#2643=VECTOR('',#9611,1.);
#2644=VECTOR('',#9612,1.);
#2645=VECTOR('',#9615,1.);
#2646=VECTOR('',#9616,1.);
#2647=VECTOR('',#9617,1.);
#2648=VECTOR('',#9620,1.);
#2649=VECTOR('',#9621,1.);
#2650=VECTOR('',#9622,1.);
#2651=VECTOR('',#9625,1.);
#2652=VECTOR('',#9626,1.);
#2653=VECTOR('',#9627,1.);
#2654=VECTOR('',#9630,1.);
#2655=VECTOR('',#9631,1.);
#3025=CIRCLE('',#7704,0.3);
#3026=CIRCLE('',#7706,0.35);
#3027=CIRCLE('',#7708,0.35);
#3028=CIRCLE('',#7710,0.32);
#3029=CIRCLE('',#7712,0.22);
#3030=CIRCLE('',#7714,0.1954);
#3031=CIRCLE('',#7716,0.1954);
#3032=CIRCLE('',#7718,0.16);
#3516=VERTEX_POINT('',#11912);
#3517=VERTEX_POINT('',#11915);
#3518=VERTEX_POINT('',#11919);
#3519=VERTEX_POINT('',#11923);
#3520=VERTEX_POINT('',#11927);
#3521=VERTEX_POINT('',#11930);
#3522=VERTEX_POINT('',#11934);
#3523=VERTEX_POINT('',#11938);
#3524=VERTEX_POINT('',#11943);
#3525=VERTEX_POINT('',#11944);
#3526=VERTEX_POINT('',#11946);
#3527=VERTEX_POINT('',#11948);
#3528=VERTEX_POINT('',#11952);
#3529=VERTEX_POINT('',#11954);
#3530=VERTEX_POINT('',#11958);
#3531=VERTEX_POINT('',#11960);
#3532=VERTEX_POINT('',#11964);
#3533=VERTEX_POINT('',#11966);
#3534=VERTEX_POINT('',#11970);
#3535=VERTEX_POINT('',#11972);
#4269=EDGE_CURVE('',#3516,#3516,#3025,.T.);
#4270=EDGE_CURVE('',#3517,#3517,#3026,.T.);
#4271=EDGE_CURVE('',#3517,#3516,#2191,.T.);
#4272=EDGE_CURVE('',#3518,#3518,#3027,.T.);
#4273=EDGE_CURVE('',#3518,#3517,#2192,.T.);
#4274=EDGE_CURVE('',#3519,#3519,#3028,.T.);
#4275=EDGE_CURVE('',#3519,#3518,#2193,.T.);
#4276=EDGE_CURVE('',#3520,#3520,#3029,.T.);
#4277=EDGE_CURVE('',#3521,#3521,#3030,.F.);
#4278=EDGE_CURVE('',#3521,#3520,#2194,.T.);
#4279=EDGE_CURVE('',#3522,#3522,#3031,.F.);
#4280=EDGE_CURVE('',#3522,#3521,#2195,.T.);
#4281=EDGE_CURVE('',#3523,#3523,#3032,.T.);
#4282=EDGE_CURVE('',#3523,#3522,#2196,.T.);
#4283=EDGE_CURVE('',#3524,#3525,#2197,.T.);
#4284=EDGE_CURVE('',#3525,#3526,#2198,.T.);
#4285=EDGE_CURVE('',#3526,#3527,#2199,.T.);
#4286=EDGE_CURVE('',#3524,#3527,#2200,.T.);
#4287=EDGE_CURVE('',#3525,#3528,#2201,.T.);
#4288=EDGE_CURVE('',#3528,#3529,#2202,.T.);
#4289=EDGE_CURVE('',#3529,#3526,#2203,.T.);
#4290=EDGE_CURVE('',#3528,#3530,#2204,.T.);
#4291=EDGE_CURVE('',#3530,#3531,#2205,.T.);
#4292=EDGE_CURVE('',#3531,#3529,#2206,.T.);
#4293=EDGE_CURVE('',#3530,#3532,#2207,.T.);
#4294=EDGE_CURVE('',#3532,#3533,#2208,.T.);
#4295=EDGE_CURVE('',#3533,#3531,#2209,.T.);
#4296=EDGE_CURVE('',#3532,#3534,#2210,.T.);
#4297=EDGE_CURVE('',#3534,#3535,#2211,.T.);
#4298=EDGE_CURVE('',#3535,#3533,#2212,.T.);
#4299=EDGE_CURVE('',#3534,#3524,#2213,.T.);
#4300=EDGE_CURVE('',#3527,#3535,#2214,.T.);
#5729=ORIENTED_EDGE('',*,*,#4269,.F.);
#5730=ORIENTED_EDGE('',*,*,#4270,.F.);
#5731=ORIENTED_EDGE('',*,*,#4271,.T.);
#5732=ORIENTED_EDGE('',*,*,#4269,.T.);
#5733=ORIENTED_EDGE('',*,*,#4271,.F.);
#5734=ORIENTED_EDGE('',*,*,#4272,.F.);
#5735=ORIENTED_EDGE('',*,*,#4273,.T.);
#5736=ORIENTED_EDGE('',*,*,#4270,.T.);
#5737=ORIENTED_EDGE('',*,*,#4273,.F.);
#5738=ORIENTED_EDGE('',*,*,#4274,.F.);
#5739=ORIENTED_EDGE('',*,*,#4275,.T.);
#5740=ORIENTED_EDGE('',*,*,#4272,.T.);
#5741=ORIENTED_EDGE('',*,*,#4275,.F.);
#5742=ORIENTED_EDGE('',*,*,#4274,.T.);
#5743=ORIENTED_EDGE('',*,*,#4276,.F.);
#5744=ORIENTED_EDGE('',*,*,#4277,.F.);
#5745=ORIENTED_EDGE('',*,*,#4278,.T.);
#5746=ORIENTED_EDGE('',*,*,#4276,.T.);
#5747=ORIENTED_EDGE('',*,*,#4278,.F.);
#5748=ORIENTED_EDGE('',*,*,#4279,.F.);
#5749=ORIENTED_EDGE('',*,*,#4280,.T.);
#5750=ORIENTED_EDGE('',*,*,#4277,.T.);
#5751=ORIENTED_EDGE('',*,*,#4280,.F.);
#5752=ORIENTED_EDGE('',*,*,#4281,.F.);
#5753=ORIENTED_EDGE('',*,*,#4282,.T.);
#5754=ORIENTED_EDGE('',*,*,#4279,.T.);
#5755=ORIENTED_EDGE('',*,*,#4282,.F.);
#5756=ORIENTED_EDGE('',*,*,#4281,.T.);
#5757=ORIENTED_EDGE('',*,*,#4283,.T.);
#5758=ORIENTED_EDGE('',*,*,#4284,.T.);
#5759=ORIENTED_EDGE('',*,*,#4285,.T.);
#5760=ORIENTED_EDGE('',*,*,#4286,.F.);
#5761=ORIENTED_EDGE('',*,*,#4287,.T.);
#5762=ORIENTED_EDGE('',*,*,#4288,.T.);
#5763=ORIENTED_EDGE('',*,*,#4289,.T.);
#5764=ORIENTED_EDGE('',*,*,#4284,.F.);
#5765=ORIENTED_EDGE('',*,*,#4290,.T.);
#5766=ORIENTED_EDGE('',*,*,#4291,.T.);
#5767=ORIENTED_EDGE('',*,*,#4292,.T.);
#5768=ORIENTED_EDGE('',*,*,#4288,.F.);
#5769=ORIENTED_EDGE('',*,*,#4293,.T.);
#5770=ORIENTED_EDGE('',*,*,#4294,.T.);
#5771=ORIENTED_EDGE('',*,*,#4295,.T.);
#5772=ORIENTED_EDGE('',*,*,#4291,.F.);
#5773=ORIENTED_EDGE('',*,*,#4296,.T.);
#5774=ORIENTED_EDGE('',*,*,#4297,.T.);
#5775=ORIENTED_EDGE('',*,*,#4298,.T.);
#5776=ORIENTED_EDGE('',*,*,#4294,.F.);
#5777=ORIENTED_EDGE('',*,*,#4299,.T.);
#5778=ORIENTED_EDGE('',*,*,#4286,.T.);
#5779=ORIENTED_EDGE('',*,*,#4300,.T.);
#5780=ORIENTED_EDGE('',*,*,#4297,.F.);
#5781=ORIENTED_EDGE('',*,*,#4299,.F.);
#5782=ORIENTED_EDGE('',*,*,#4296,.F.);
#5783=ORIENTED_EDGE('',*,*,#4293,.F.);
#5784=ORIENTED_EDGE('',*,*,#4290,.F.);
#5785=ORIENTED_EDGE('',*,*,#4287,.F.);
#5786=ORIENTED_EDGE('',*,*,#4283,.F.);
#5787=ORIENTED_EDGE('',*,*,#4300,.F.);
#5788=ORIENTED_EDGE('',*,*,#4285,.F.);
#5789=ORIENTED_EDGE('',*,*,#4289,.F.);
#5790=ORIENTED_EDGE('',*,*,#4292,.F.);
#5791=ORIENTED_EDGE('',*,*,#4295,.F.);
#5792=ORIENTED_EDGE('',*,*,#4298,.F.);
#6144=CYLINDRICAL_SURFACE('',#7707,0.35);
#6145=CYLINDRICAL_SURFACE('',#7715,0.1954);
#6492=ADVANCED_FACE('',(#1217),#836,.T.);
#6493=ADVANCED_FACE('',(#1218),#320,.T.);
#6494=ADVANCED_FACE('',(#1219),#6144,.T.);
#6495=ADVANCED_FACE('',(#1220),#321,.T.);
#6496=ADVANCED_FACE('',(#1221,#635),#837,.T.);
#6497=ADVANCED_FACE('',(#1222),#322,.T.);
#6498=ADVANCED_FACE('',(#1223),#6145,.T.);
#6499=ADVANCED_FACE('',(#1224),#323,.T.);
#6500=ADVANCED_FACE('',(#1225),#838,.T.);
#6501=ADVANCED_FACE('',(#1226),#839,.F.);
#6502=ADVANCED_FACE('',(#1227),#840,.F.);
#6503=ADVANCED_FACE('',(#1228),#841,.F.);
#6504=ADVANCED_FACE('',(#1229),#842,.F.);
#6505=ADVANCED_FACE('',(#1230),#843,.F.);
#6506=ADVANCED_FACE('',(#1231),#844,.F.);
#6507=ADVANCED_FACE('',(#1232),#845,.F.);
#6508=ADVANCED_FACE('',(#1233),#846,.F.);
#6610=CLOSED_SHELL('',(#6492,#6493,#6494,#6495,#6496,#6497,#6498,#6499,
#6500));
#6611=CLOSED_SHELL('',(#6501,#6502,#6503,#6504,#6505,#6506,#6507,#6508));
#7702=AXIS2_PLACEMENT_3D('',#11910,#9560,#9561);
#7703=AXIS2_PLACEMENT_3D('',#11911,#9562,#9563);
#7704=AXIS2_PLACEMENT_3D('',#11913,#9564,#9565);
#7705=AXIS2_PLACEMENT_3D('',#11914,#9566,#9567);
#7706=AXIS2_PLACEMENT_3D('',#11916,#9568,#9569);
#7707=AXIS2_PLACEMENT_3D('',#11918,#9571,#9572);
#7708=AXIS2_PLACEMENT_3D('',#11920,#9573,#9574);
#7709=AXIS2_PLACEMENT_3D('',#11922,#9576,#9577);
#7710=AXIS2_PLACEMENT_3D('',#11924,#9578,#9579);
#7711=AXIS2_PLACEMENT_3D('',#11926,#9581,#9582);
#7712=AXIS2_PLACEMENT_3D('',#11928,#9583,#9584);
#7713=AXIS2_PLACEMENT_3D('',#11929,#9585,#9586);
#7714=AXIS2_PLACEMENT_3D('',#11931,#9587,#9588);
#7715=AXIS2_PLACEMENT_3D('',#11933,#9590,#9591);
#7716=AXIS2_PLACEMENT_3D('',#11935,#9592,#9593);
#7717=AXIS2_PLACEMENT_3D('',#11937,#9595,#9596);
#7718=AXIS2_PLACEMENT_3D('',#11939,#9597,#9598);
#7719=AXIS2_PLACEMENT_3D('',#11941,#9600,#9601);
#7720=AXIS2_PLACEMENT_3D('',#11942,#9602,#9603);
#7721=AXIS2_PLACEMENT_3D('',#11951,#9608,#9609);
#7722=AXIS2_PLACEMENT_3D('',#11957,#9613,#9614);
#7723=AXIS2_PLACEMENT_3D('',#11963,#9618,#9619);
#7724=AXIS2_PLACEMENT_3D('',#11969,#9623,#9624);
#7725=AXIS2_PLACEMENT_3D('',#11975,#9628,#9629);
#7726=AXIS2_PLACEMENT_3D('',#11978,#9632,#9633);
#7727=AXIS2_PLACEMENT_3D('',#11979,#9634,#9635);
#9560=DIRECTION('axis',(0.,0.,1.));
#9561=DIRECTION('refdir',(1.,0.,0.));
#9562=DIRECTION('center_axis',(0.,1.,0.));
#9563=DIRECTION('ref_axis',(0.,0.,1.));
#9564=DIRECTION('center_axis',(0.,-1.,0.));
#9565=DIRECTION('ref_axis',(1.,0.,0.));
#9566=DIRECTION('center_axis',(0.,-1.,0.));
#9567=DIRECTION('ref_axis',(1.,0.,0.));
#9568=DIRECTION('center_axis',(0.,-1.,0.));
#9569=DIRECTION('ref_axis',(1.,0.,0.));
#9570=DIRECTION('',(0.707106781186547,0.707106781186548,8.65956056235493E-17));
#9571=DIRECTION('center_axis',(0.,-1.,0.));
#9572=DIRECTION('ref_axis',(1.,0.,0.));
#9573=DIRECTION('center_axis',(0.,-1.,0.));
#9574=DIRECTION('ref_axis',(1.,0.,0.));
#9575=DIRECTION('',(0.,1.,0.));
#9576=DIRECTION('center_axis',(0.,1.,0.));
#9577=DIRECTION('ref_axis',(1.,0.,0.));
#9578=DIRECTION('center_axis',(0.,-1.,0.));
#9579=DIRECTION('ref_axis',(1.,0.,0.));
#9580=DIRECTION('',(-0.707106781186547,0.707106781186548,-8.65956056235493E-17));
#9581=DIRECTION('center_axis',(0.,-1.,0.));
#9582=DIRECTION('ref_axis',(0.,0.,-1.));
#9583=DIRECTION('center_axis',(0.,-1.,0.));
#9584=DIRECTION('ref_axis',(1.,0.,0.));
#9585=DIRECTION('center_axis',(0.,1.,0.));
#9586=DIRECTION('ref_axis',(1.,0.,0.));
#9587=DIRECTION('center_axis',(0.,1.,0.));
#9588=DIRECTION('ref_axis',(1.,0.,0.));
#9589=DIRECTION('',(-0.447213595499958,0.894427190999916,-5.47678698264203E-17));
#9590=DIRECTION('center_axis',(0.,-1.,0.));
#9591=DIRECTION('ref_axis',(1.,0.,0.));
#9592=DIRECTION('center_axis',(0.,1.,0.));
#9593=DIRECTION('ref_axis',(1.,0.,0.));
#9594=DIRECTION('',(0.,1.,0.));
#9595=DIRECTION('center_axis',(0.,1.,0.));
#9596=DIRECTION('ref_axis',(1.,0.,0.));
#9597=DIRECTION('center_axis',(0.,-1.,0.));
#9598=DIRECTION('ref_axis',(1.,0.,0.));
#9599=DIRECTION('',(-0.707106781186547,0.707106781186548,-8.65956056235493E-17));
#9600=DIRECTION('center_axis',(0.,-1.,0.));
#9601=DIRECTION('ref_axis',(0.,0.,-1.));
#9602=DIRECTION('center_axis',(0.866025403784439,0.,-0.5));
#9603=DIRECTION('ref_axis',(0.5,0.,0.866025403784439));
#9604=DIRECTION('',(-0.5,0.,-0.866025403784439));
#9605=DIRECTION('',(0.,-1.,0.));
#9606=DIRECTION('',(0.5,0.,0.866025403784439));
#9607=DIRECTION('',(0.,-1.,0.));
#9608=DIRECTION('center_axis',(1.60246890531964E-16,0.,-1.));
#9609=DIRECTION('ref_axis',(1.,0.,1.60246890531964E-16));
#9610=DIRECTION('',(-1.,0.,-1.60246890531964E-16));
#9611=DIRECTION('',(0.,-1.,0.));
#9612=DIRECTION('',(1.,0.,1.60246890531964E-16));
#9613=DIRECTION('center_axis',(-0.866025403784439,0.,-0.5));
#9614=DIRECTION('ref_axis',(0.5,0.,-0.866025403784439));
#9615=DIRECTION('',(-0.5,0.,0.866025403784439));
#9616=DIRECTION('',(0.,-1.,0.));
#9617=DIRECTION('',(0.5,0.,-0.866025403784439));
#9618=DIRECTION('center_axis',(-0.866025403784439,0.,0.5));
#9619=DIRECTION('ref_axis',(-0.5,0.,-0.866025403784439));
#9620=DIRECTION('',(0.5,0.,0.866025403784439));
#9621=DIRECTION('',(0.,-1.,0.));
#9622=DIRECTION('',(-0.5,0.,-0.866025403784439));
#9623=DIRECTION('center_axis',(-1.60246890531964E-16,0.,1.));
#9624=DIRECTION('ref_axis',(-1.,0.,-1.60246890531964E-16));
#9625=DIRECTION('',(1.,0.,1.60246890531964E-16));
#9626=DIRECTION('',(0.,-1.,0.));
#9627=DIRECTION('',(-1.,0.,-1.60246890531964E-16));
#9628=DIRECTION('center_axis',(0.866025403784439,0.,0.5));
#9629=DIRECTION('ref_axis',(-0.5,0.,0.866025403784439));
#9630=DIRECTION('',(0.5,0.,-0.866025403784439));
#9631=DIRECTION('',(-0.5,0.,0.866025403784439));
#9632=DIRECTION('center_axis',(0.,1.,0.));
#9633=DIRECTION('ref_axis',(1.,0.,0.));
#9634=DIRECTION('center_axis',(0.,-1.,0.));
#9635=DIRECTION('ref_axis',(0.,0.,-1.));
#11910=CARTESIAN_POINT('',(0.,0.,0.));
#11911=CARTESIAN_POINT('Origin',(0.3,0.4,0.));
#11912=CARTESIAN_POINT('',(-0.3,0.4,-3.67394039744206E-17));
#11913=CARTESIAN_POINT('Origin',(0.,0.4,0.));
#11914=CARTESIAN_POINT('Origin',(0.,0.375,0.));
#11915=CARTESIAN_POINT('',(-0.35,0.35,-4.28626379701573E-17));
#11916=CARTESIAN_POINT('Origin',(0.,0.35,0.));
#11917=CARTESIAN_POINT('',(-0.325,0.375,-3.9801020972289E-17));
#11918=CARTESIAN_POINT('Origin',(0.,0.19,0.));
#11919=CARTESIAN_POINT('',(-0.35,0.03,-4.28626379701574E-17));
#11920=CARTESIAN_POINT('Origin',(0.,0.03,0.));
#11921=CARTESIAN_POINT('',(-0.35,0.19,-4.28626379701574E-17));
#11922=CARTESIAN_POINT('Origin',(0.,0.0149999999999999,0.));
#11923=CARTESIAN_POINT('',(-0.32,-3.29597460435593E-17,-3.91886975727153E-17));
#11924=CARTESIAN_POINT('Origin',(0.,0.,0.));
#11925=CARTESIAN_POINT('',(-0.335,0.0149999999999999,-4.10256677714363E-17));
#11926=CARTESIAN_POINT('Origin',(0.22,0.,0.));
#11927=CARTESIAN_POINT('',(-0.22,-6.93889390390723E-18,-2.69422295812418E-17));
#11928=CARTESIAN_POINT('Origin',(0.,0.,0.));
#11929=CARTESIAN_POINT('Origin',(0.,-0.02,0.));
#11930=CARTESIAN_POINT('',(-0.1954,-0.0492,2.39295984553393E-17));
#11931=CARTESIAN_POINT('Origin',(0.,-0.0492,0.));
#11932=CARTESIAN_POINT('',(-0.21,-0.02,-2.57175827820944E-17));
#11933=CARTESIAN_POINT('Origin',(0.,-0.8,0.));
#11934=CARTESIAN_POINT('',(-0.1954,-1.5646,2.39295984553393E-17));
#11935=CARTESIAN_POINT('Origin',(0.,-1.5646,0.));
#11936=CARTESIAN_POINT('',(-0.1954,-0.8,-2.39295984553393E-17));
#11937=CARTESIAN_POINT('Origin',(0.,-1.58,0.));
#11938=CARTESIAN_POINT('',(-0.16,-1.6,-1.95943487863577E-17));
#11939=CARTESIAN_POINT('Origin',(0.,-1.6,0.));
#11940=CARTESIAN_POINT('',(-0.18,-1.58,-2.20436423846524E-17));
#11941=CARTESIAN_POINT('Origin',(0.,-1.6,0.));
#11942=CARTESIAN_POINT('Origin',(0.0866025403784439,-0.4,-0.15));
#11943=CARTESIAN_POINT('',(0.173205080756888,-0.4,0.));
#11944=CARTESIAN_POINT('',(0.0866025403784439,-0.4,-0.15));
#11945=CARTESIAN_POINT('',(0.173205080756888,-0.4,0.));
#11946=CARTESIAN_POINT('',(0.0866025403784439,-0.64,-0.15));
#11947=CARTESIAN_POINT('',(0.0866025403784439,-0.4,-0.15));
#11948=CARTESIAN_POINT('',(0.173205080756888,-0.64,0.));
#11949=CARTESIAN_POINT('',(0.173205080756888,-0.64,0.));
#11950=CARTESIAN_POINT('',(0.173205080756888,-0.4,0.));
#11951=CARTESIAN_POINT('Origin',(-0.0866025403784438,-0.4,-0.15));
#11952=CARTESIAN_POINT('',(-0.0866025403784438,-0.4,-0.15));
#11953=CARTESIAN_POINT('',(0.0866025403784439,-0.4,-0.15));
#11954=CARTESIAN_POINT('',(-0.0866025403784438,-0.64,-0.15));
#11955=CARTESIAN_POINT('',(-0.0866025403784438,-0.4,-0.15));
#11956=CARTESIAN_POINT('',(0.0866025403784439,-0.64,-0.15));
#11957=CARTESIAN_POINT('Origin',(-0.173205080756888,-0.4,-2.77555756156289E-17));
#11958=CARTESIAN_POINT('',(-0.173205080756888,-0.4,-2.12115047744981E-17));
#11959=CARTESIAN_POINT('',(-0.0866025403784438,-0.4,-0.15));
#11960=CARTESIAN_POINT('',(-0.173205080756888,-0.64,-2.77555756156289E-17));
#11961=CARTESIAN_POINT('',(-0.173205080756888,-0.4,-2.12115047744981E-17));
#11962=CARTESIAN_POINT('',(-0.0866025403784438,-0.64,-0.15));
#11963=CARTESIAN_POINT('Origin',(-0.0866025403784439,-0.4,0.15));
#11964=CARTESIAN_POINT('',(-0.0866025403784439,-0.4,0.15));
#11965=CARTESIAN_POINT('',(-0.173205080756888,-0.4,-2.12115047744981E-17));
#11966=CARTESIAN_POINT('',(-0.0866025403784439,-0.64,0.15));
#11967=CARTESIAN_POINT('',(-0.0866025403784439,-0.4,0.15));
#11968=CARTESIAN_POINT('',(-0.173205080756888,-0.64,-2.12115047744981E-17));
#11969=CARTESIAN_POINT('Origin',(0.0866025403784439,-0.4,0.15));
#11970=CARTESIAN_POINT('',(0.0866025403784439,-0.4,0.15));
#11971=CARTESIAN_POINT('',(-0.0866025403784439,-0.4,0.15));
#11972=CARTESIAN_POINT('',(0.0866025403784439,-0.64,0.15));
#11973=CARTESIAN_POINT('',(0.0866025403784439,-0.4,0.15));
#11974=CARTESIAN_POINT('',(-0.0866025403784439,-0.64,0.15));
#11975=CARTESIAN_POINT('Origin',(0.173205080756888,-0.4,0.));
#11976=CARTESIAN_POINT('',(0.0866025403784439,-0.4,0.15));
#11977=CARTESIAN_POINT('',(0.0866025403784439,-0.64,0.15));
#11978=CARTESIAN_POINT('Origin',(0.,-0.4,-2.77555756156289E-17));
#11979=CARTESIAN_POINT('Origin',(0.,-0.64,-2.77555756156289E-17));
#12357=UNCERTAINTY_MEASURE_WITH_UNIT(LENGTH_MEASURE(0.001),#12414,
'DISTANCE_ACCURACY_VALUE',
'Maximum model space distance between geometric entities at asserted c
onnectivities');
#12367=UNCERTAINTY_MEASURE_WITH_UNIT(LENGTH_MEASURE(0.001),#12414,
'DISTANCE_ACCURACY_VALUE',
'Maximum model space distance between geometric entities at asserted c
onnectivities');
#12403=(
GEOMETRIC_REPRESENTATION_CONTEXT(3)
GLOBAL_UNCERTAINTY_ASSIGNED_CONTEXT((#12357))
GLOBAL_UNIT_ASSIGNED_CONTEXT((#12414,#12416,#12417))
REPRESENTATION_CONTEXT('','3D')
);
#12413=(
GEOMETRIC_REPRESENTATION_CONTEXT(3)
GLOBAL_UNCERTAINTY_ASSIGNED_CONTEXT((#12367))
GLOBAL_UNIT_ASSIGNED_CONTEXT((#12414,#12416,#12417))
REPRESENTATION_CONTEXT('','3D')
);
#12414=(
LENGTH_UNIT()
NAMED_UNIT(*)
SI_UNIT(.CENTI.,.METRE.)
);
#12416=(
NAMED_UNIT(*)
PLANE_ANGLE_UNIT()
SI_UNIT($,.RADIAN.)
);
#12417=(
NAMED_UNIT(*)
SI_UNIT($,.STERADIAN.)
SOLID_ANGLE_UNIT()
);
#12453=SHAPE_DEFINITION_REPRESENTATION(#12505,#12606);
#12505=PRODUCT_DEFINITION_SHAPE('',$,#12652);
#12606=SHAPE_REPRESENTATION('',(#7702),#12403);
#12616=PRODUCT_DEFINITION_CONTEXT('part definition',#12753,'design');
#12652=PRODUCT_DEFINITION('Cap Screw - M4x16','Cap Screw - M4x16',#12697,
#12616);
#12697=PRODUCT_DEFINITION_FORMATION('',$,#12790);
#12753=APPLICATION_CONTEXT(
'Core Data for Automotive Mechanical Design Process');
#12754=PRODUCT_CONTEXT('part definition',#12753,'mechanical');
#12790=PRODUCT('Cap Screw - M4x16','Cap Screw - M4x16',
'Cap Screw - M4x16',(#12754));
#12870=COLOUR_RGB('Black',0.12,0.14,0.17);
#12871=FILL_AREA_STYLE_COLOUR('',#12870);
#12872=FILL_AREA_STYLE('',(#12871));
#12873=SURFACE_STYLE_FILL_AREA(#12872);
#12874=SURFACE_SIDE_STYLE('',(#12873));
#12875=SURFACE_STYLE_USAGE(.BOTH.,#12874);
#12876=PRESENTATION_STYLE_ASSIGNMENT((#12875));
ENDSEC;
END-ISO-10303-21;
